ISO-10303-21;
HEADER;
/* Generated by software containing ST-Developer
 * from STEP Tools, Inc. (www.steptools.com) 
 */

FILE_DESCRIPTION(
/* description */ (''),
/* implementation_level */ '2;1');

FILE_NAME(
/* name */ 'Pin_01.step',
/* time_stamp */ '2026-10-05T21:34:53-07:00',
/* author */ (''),
/* organization */ (''),
/* preprocessor_version */ 'ST-DEVELOPER v20.2',
/* originating_system */ 'Autodesk Translation Framework v15.15.0.0',
/* authorisation */ '');

FILE_SCHEMA (('AUTOMOTIVE_DESIGN { 1 0 10303 214 3 1 1 }'));
ENDSEC;

DATA;
#10=MECHANICAL_DESIGN_GEOMETRIC_PRESENTATION_REPRESENTATION('',(#73),#9822);
#55=SHAPE_REPRESENTATION_RELATIONSHIP('SRR','None',#9865,#64);
#64=ADVANCED_BREP_SHAPE_REPRESENTATION('',(#82),#9821);
#73=STYLED_ITEM('',(#9912),#82);
#82=MANIFOLD_SOLID_BREP('Body1',#3296);
#261=PLANE('',#3708);
#262=PLANE('',#3711);
#263=PLANE('',#3716);
#264=PLANE('',#3717);
#444=FACE_OUTER_BOUND('',#645,.T.);
#445=FACE_OUTER_BOUND('',#646,.T.);
#446=FACE_OUTER_BOUND('',#647,.T.);
#447=FACE_OUTER_BOUND('',#648,.T.);
#448=FACE_OUTER_BOUND('',#649,.T.);
#449=FACE_OUTER_BOUND('',#650,.T.);
#645=EDGE_LOOP('',(#3002,#3003,#3004,#3005));
#646=EDGE_LOOP('',(#3006,#3007,#3008,#3009));
#647=EDGE_LOOP('',(#3010,#3011,#3012,#3013));
#648=EDGE_LOOP('',(#3014,#3015,#3016,#3017));
#649=EDGE_LOOP('',(#3018,#3019,#3020,#3021));
#650=EDGE_LOOP('',(#3022,#3023,#3024,#3025));
#902=LINE('',#9771,#1161);
#903=LINE('',#9774,#1162);
#904=LINE('',#9777,#1163);
#905=LINE('',#9779,#1164);
#906=LINE('',#9780,#1165);
#907=LINE('',#9783,#1166);
#908=LINE('',#9788,#1167);
#909=LINE('',#9790,#1168);
#1161=VECTOR('',#4604,10.);
#1162=VECTOR('',#4607,10.);
#1163=VECTOR('',#4610,10.);
#1164=VECTOR('',#4611,10.);
#1165=VECTOR('',#4612,10.);
#1166=VECTOR('',#4615,10.);
#1167=VECTOR('',#4622,10.);
#1168=VECTOR('',#4625,10.);
#1315=CIRCLE('',#3709,1.);
#1316=CIRCLE('',#3710,1.);
#1317=CIRCLE('',#3713,1.);
#1318=CIRCLE('',#3715,1.);
#1617=VERTEX_POINT('',#9767);
#1618=VERTEX_POINT('',#9768);
#1619=VERTEX_POINT('',#9770);
#1620=VERTEX_POINT('',#9772);
#1621=VERTEX_POINT('',#9776);
#1622=VERTEX_POINT('',#9778);
#1623=VERTEX_POINT('',#9782);
#1624=VERTEX_POINT('',#9786);
#2080=EDGE_CURVE('',#1617,#1618,#1315,.T.);
#2081=EDGE_CURVE('',#1619,#1617,#902,.T.);
#2082=EDGE_CURVE('',#1620,#1619,#1316,.T.);
#2083=EDGE_CURVE('',#1618,#1620,#903,.T.);
#2084=EDGE_CURVE('',#1617,#1621,#904,.T.);
#2085=EDGE_CURVE('',#1622,#1621,#905,.T.);
#2086=EDGE_CURVE('',#1619,#1622,#906,.T.);
#2087=EDGE_CURVE('',#1618,#1623,#907,.T.);
#2088=EDGE_CURVE('',#1621,#1623,#1317,.T.);
#2089=EDGE_CURVE('',#1624,#1622,#1318,.T.);
#2090=EDGE_CURVE('',#1620,#1624,#908,.T.);
#2091=EDGE_CURVE('',#1623,#1624,#909,.T.);
#3002=ORIENTED_EDGE('',*,*,#2080,.F.);
#3003=ORIENTED_EDGE('',*,*,#2081,.F.);
#3004=ORIENTED_EDGE('',*,*,#2082,.F.);
#3005=ORIENTED_EDGE('',*,*,#2083,.F.);
#3006=ORIENTED_EDGE('',*,*,#2081,.T.);
#3007=ORIENTED_EDGE('',*,*,#2084,.T.);
#3008=ORIENTED_EDGE('',*,*,#2085,.F.);
#3009=ORIENTED_EDGE('',*,*,#2086,.F.);
#3010=ORIENTED_EDGE('',*,*,#2080,.T.);
#3011=ORIENTED_EDGE('',*,*,#2087,.T.);
#3012=ORIENTED_EDGE('',*,*,#2088,.F.);
#3013=ORIENTED_EDGE('',*,*,#2084,.F.);
#3014=ORIENTED_EDGE('',*,*,#2082,.T.);
#3015=ORIENTED_EDGE('',*,*,#2086,.T.);
#3016=ORIENTED_EDGE('',*,*,#2089,.F.);
#3017=ORIENTED_EDGE('',*,*,#2090,.F.);
#3018=ORIENTED_EDGE('',*,*,#2083,.T.);
#3019=ORIENTED_EDGE('',*,*,#2090,.T.);
#3020=ORIENTED_EDGE('',*,*,#2091,.F.);
#3021=ORIENTED_EDGE('',*,*,#2087,.F.);
#3022=ORIENTED_EDGE('',*,*,#2088,.T.);
#3023=ORIENTED_EDGE('',*,*,#2091,.T.);
#3024=ORIENTED_EDGE('',*,*,#2089,.T.);
#3025=ORIENTED_EDGE('',*,*,#2085,.T.);
#3101=CYLINDRICAL_SURFACE('',#3712,1.);
#3102=CYLINDRICAL_SURFACE('',#3714,1.);
#3282=ADVANCED_FACE('',(#444),#261,.T.);
#3283=ADVANCED_FACE('',(#445),#262,.T.);
#3284=ADVANCED_FACE('',(#446),#3101,.T.);
#3285=ADVANCED_FACE('',(#447),#3102,.T.);
#3286=ADVANCED_FACE('',(#448),#263,.T.);
#3287=ADVANCED_FACE('',(#449),#264,.F.);
#3296=CLOSED_SHELL('',(#3282,#3283,#3284,#3285,#3286,#3287));
#3707=AXIS2_PLACEMENT_3D('',#9765,#4598,#4599);
#3708=AXIS2_PLACEMENT_3D('',#9766,#4600,#4601);
#3709=AXIS2_PLACEMENT_3D('',#9769,#4602,#4603);
#3710=AXIS2_PLACEMENT_3D('',#9773,#4605,#4606);
#3711=AXIS2_PLACEMENT_3D('',#9775,#4608,#4609);
#3712=AXIS2_PLACEMENT_3D('',#9781,#4613,#4614);
#3713=AXIS2_PLACEMENT_3D('',#9784,#4616,#4617);
#3714=AXIS2_PLACEMENT_3D('',#9785,#4618,#4619);
#3715=AXIS2_PLACEMENT_3D('',#9787,#4620,#4621);
#3716=AXIS2_PLACEMENT_3D('',#9789,#4623,#4624);
#3717=AXIS2_PLACEMENT_3D('',#9791,#4626,#4627);
#4598=DIRECTION('axis',(0.,0.,1.));
#4599=DIRECTION('refdir',(1.,0.,0.));
#4600=DIRECTION('center_axis',(0.,1.,0.));
#4601=DIRECTION('ref_axis',(1.,0.,0.));
#4602=DIRECTION('center_axis',(0.,-1.,0.));
#4603=DIRECTION('ref_axis',(1.,0.,0.));
#4604=DIRECTION('',(0.,0.,-1.));
#4605=DIRECTION('center_axis',(0.,-1.,0.));
#4606=DIRECTION('ref_axis',(-1.,0.,0.));
#4607=DIRECTION('',(0.,0.,1.));
#4608=DIRECTION('center_axis',(-1.,0.,0.));
#4609=DIRECTION('ref_axis',(0.,0.,-1.));
#4610=DIRECTION('',(0.,-1.,0.));
#4611=DIRECTION('',(0.,0.,-1.));
#4612=DIRECTION('',(0.,-1.,0.));
#4613=DIRECTION('center_axis',(0.,-1.,0.));
#4614=DIRECTION('ref_axis',(1.,0.,0.));
#4615=DIRECTION('',(0.,-1.,0.));
#4616=DIRECTION('center_axis',(0.,-1.,0.));
#4617=DIRECTION('ref_axis',(1.,0.,0.));
#4618=DIRECTION('center_axis',(0.,-1.,0.));
#4619=DIRECTION('ref_axis',(-1.,0.,0.));
#4620=DIRECTION('center_axis',(0.,-1.,0.));
#4621=DIRECTION('ref_axis',(-1.,0.,0.));
#4622=DIRECTION('',(0.,-1.,0.));
#4623=DIRECTION('center_axis',(1.,0.,0.));
#4624=DIRECTION('ref_axis',(0.,0.,1.));
#4625=DIRECTION('',(0.,0.,1.));
#4626=DIRECTION('center_axis',(0.,1.,0.));
#4627=DIRECTION('ref_axis',(1.,0.,0.));
#9765=CARTESIAN_POINT('',(0.,0.,0.));
#9766=CARTESIAN_POINT('Origin',(0.,-4.,10.5));
#9767=CARTESIAN_POINT('',(-1.,-4.,6.5));
#9768=CARTESIAN_POINT('',(1.,-4.,6.5));
#9769=CARTESIAN_POINT('Origin',(0.,-4.,6.5));
#9770=CARTESIAN_POINT('',(-1.,-4.,14.5));
#9771=CARTESIAN_POINT('',(-1.,-4.,12.5));
#9772=CARTESIAN_POINT('',(1.,-4.,14.5));
#9773=CARTESIAN_POINT('Origin',(0.,-4.,14.5));
#9774=CARTESIAN_POINT('',(1.,-4.,8.5));
#9775=CARTESIAN_POINT('Origin',(-1.,0.,14.5));
#9776=CARTESIAN_POINT('',(-1.,-6.,6.5));
#9777=CARTESIAN_POINT('',(-1.,0.,6.5));
#9778=CARTESIAN_POINT('',(-1.,-6.,14.5));
#9779=CARTESIAN_POINT('',(-1.,-6.,6.5));
#9780=CARTESIAN_POINT('',(-1.,0.,14.5));
#9781=CARTESIAN_POINT('Origin',(0.,0.,6.5));
#9782=CARTESIAN_POINT('',(1.,-6.,6.5));
#9783=CARTESIAN_POINT('',(1.,0.,6.5));
#9784=CARTESIAN_POINT('Origin',(0.,-6.,6.5));
#9785=CARTESIAN_POINT('Origin',(0.,0.,14.5));
#9786=CARTESIAN_POINT('',(1.,-6.,14.5));
#9787=CARTESIAN_POINT('Origin',(0.,-6.,14.5));
#9788=CARTESIAN_POINT('',(1.,0.,14.5));
#9789=CARTESIAN_POINT('Origin',(1.,0.,6.5));
#9790=CARTESIAN_POINT('',(1.,-6.,14.5));
#9791=CARTESIAN_POINT('Origin',(0.,-6.,10.5));
#9810=UNCERTAINTY_MEASURE_WITH_UNIT(LENGTH_MEASURE(0.01),#9823,
'DISTANCE_ACCURACY_VALUE',
'Maximum model space distance between geometric entities at asserted c
onnectivities');
#9811=UNCERTAINTY_MEASURE_WITH_UNIT(LENGTH_MEASURE(0.01),#9823,
'DISTANCE_ACCURACY_VALUE',
'Maximum model space distance between geometric entities at asserted c
onnectivities');
#9821=(
GEOMETRIC_REPRESENTATION_CONTEXT(3)
GLOBAL_UNCERTAINTY_ASSIGNED_CONTEXT((#9810))
GLOBAL_UNIT_ASSIGNED_CONTEXT((#9823,#9825,#9826))
REPRESENTATION_CONTEXT('','3D')
);
#9822=(
GEOMETRIC_REPRESENTATION_CONTEXT(3)
GLOBAL_UNCERTAINTY_ASSIGNED_CONTEXT((#9811))
GLOBAL_UNIT_ASSIGNED_CONTEXT((#9823,#9825,#9826))
REPRESENTATION_CONTEXT('','3D')
);
#9823=(
LENGTH_UNIT()
NAMED_UNIT(*)
SI_UNIT(.MILLI.,.METRE.)
);
#9825=(
NAMED_UNIT(*)
PLANE_ANGLE_UNIT()
SI_UNIT($,.RADIAN.)
);
#9826=(
NAMED_UNIT(*)
SI_UNIT($,.STERADIAN.)
SOLID_ANGLE_UNIT()
);
#9836=SHAPE_DEFINITION_REPRESENTATION(#9846,#9865);
#9846=PRODUCT_DEFINITION_SHAPE('',$,#9876);
#9865=SHAPE_REPRESENTATION('',(#3707),#9821);
#9866=PRODUCT_DEFINITION_CONTEXT('part definition',#9898,'design');
#9876=PRODUCT_DEFINITION('Pin_01','Pin_01',#9886,#9866);
#9886=PRODUCT_DEFINITION_FORMATION('',$,#9909);
#9898=APPLICATION_CONTEXT(
'Core Data for Automotive Mechanical Design Process');
#9899=PRODUCT_CONTEXT('part definition',#9898,'mechanical');
#9909=PRODUCT('Pin_01','Pin_01',$,(#9899));
#9912=PRESENTATION_STYLE_ASSIGNMENT((#9915));
#9915=SURFACE_STYLE_USAGE(.BOTH.,#9918);
#9918=SURFACE_SIDE_STYLE('',(#9921));
#9921=SURFACE_STYLE_FILL_AREA(#9924);
#9924=FILL_AREA_STYLE('Opaque(233,233,233)',(#9927));
#9927=FILL_AREA_STYLE_COLOUR('Opaque(233,233,233)',#9930);
#9930=COLOUR_RGB('Opaque(233,233,233)', 0.40784314, 0.44705882, 0.49803922);
ENDSEC;
END-ISO-10303-21;
